ISO-10303-21;
HEADER;
/* Generated by software containing ST-Developer
 * from STEP Tools, Inc. (www.steptools.com) 
 */

FILE_DESCRIPTION(
/* description */ ('XY cross-slide table'),
/* implementation_level */ '2;1');

FILE_NAME(
/* name */ 'Flat Washer - M5.step',
/* time_stamp */ '2026-10-28T03:22:46-07:00',
/* author */ (''),
/* organization */ (''),
/* preprocessor_version */ 'ST-DEVELOPER v20.2',
/* originating_system */ 'Autodesk Translation Framework v15.17.0.0',
/* authorisation */ '');

FILE_SCHEMA (('AUTOMOTIVE_DESIGN { 1 0 10303 214 3 1 1 }'));
ENDSEC;

DATA;
#10=MECHANICAL_DESIGN_GEOMETRIC_PRESENTATION_REPRESENTATION('',(#1712),#62984);
#1449=CONICAL_SURFACE('',#24714,0.275,0.785398163397449);
#1531=SHAPE_REPRESENTATION_RELATIONSHIP('SRR','None',#63383,#1614);
#1614=ADVANCED_BREP_SHAPE_REPRESENTATION('',(#1825),#62920);
#1712=STYLED_ITEM('',(#63919),#1825);
#1825=MANIFOLD_SOLID_BREP('Body1',#23006);
#2046=FACE_BOUND('',#4682,.T.);
#2047=FACE_BOUND('',#4685,.T.);
#2477=PLANE('',#24719);
#2478=PLANE('',#24723);
#3206=FACE_OUTER_BOUND('',#4679,.T.);
#3207=FACE_OUTER_BOUND('',#4680,.T.);
#3208=FACE_OUTER_BOUND('',#4681,.T.);
#3209=FACE_OUTER_BOUND('',#4683,.T.);
#3210=FACE_OUTER_BOUND('',#4684,.T.);
#4679=EDGE_LOOP('',(#16420,#16421,#16422,#16423));
#4680=EDGE_LOOP('',(#16424,#16425,#16426,#16427));
#4681=EDGE_LOOP('',(#16428));
#4682=EDGE_LOOP('',(#16429));
#4683=EDGE_LOOP('',(#16430,#16431,#16432,#16433));
#4684=EDGE_LOOP('',(#16434));
#4685=EDGE_LOOP('',(#16435));
#6303=LINE('',#35169,#7790);
#6304=LINE('',#35173,#7791);
#6305=LINE('',#35180,#7792);
#7790=VECTOR('',#28290,0.275);
#7791=VECTOR('',#28295,0.265);
#7792=VECTOR('',#28304,0.5);
#9209=CIRCLE('',#24715,0.285);
#9210=CIRCLE('',#24716,0.265);
#9211=CIRCLE('',#24718,0.265);
#9212=CIRCLE('',#24720,0.5);
#9213=CIRCLE('',#24722,0.5);
#10293=VERTEX_POINT('',#35166);
#10294=VERTEX_POINT('',#35168);
#10295=VERTEX_POINT('',#35172);
#10296=VERTEX_POINT('',#35176);
#10297=VERTEX_POINT('',#35179);
#12594=EDGE_CURVE('',#10293,#10293,#9209,.T.);
#12595=EDGE_CURVE('',#10293,#10294,#6303,.T.);
#12596=EDGE_CURVE('',#10294,#10294,#9210,.T.);
#12597=EDGE_CURVE('',#10294,#10295,#6304,.T.);
#12598=EDGE_CURVE('',#10295,#10295,#9211,.T.);
#12599=EDGE_CURVE('',#10296,#10296,#9212,.T.);
#12600=EDGE_CURVE('',#10296,#10297,#6305,.T.);
#12601=EDGE_CURVE('',#10297,#10297,#9213,.T.);
#16420=ORIENTED_EDGE('',*,*,#12594,.T.);
#16421=ORIENTED_EDGE('',*,*,#12595,.T.);
#16422=ORIENTED_EDGE('',*,*,#12596,.T.);
#16423=ORIENTED_EDGE('',*,*,#12595,.F.);
#16424=ORIENTED_EDGE('',*,*,#12596,.F.);
#16425=ORIENTED_EDGE('',*,*,#12597,.T.);
#16426=ORIENTED_EDGE('',*,*,#12598,.T.);
#16427=ORIENTED_EDGE('',*,*,#12597,.F.);
#16428=ORIENTED_EDGE('',*,*,#12599,.T.);
#16429=ORIENTED_EDGE('',*,*,#12594,.F.);
#16430=ORIENTED_EDGE('',*,*,#12599,.F.);
#16431=ORIENTED_EDGE('',*,*,#12600,.T.);
#16432=ORIENTED_EDGE('',*,*,#12601,.T.);
#16433=ORIENTED_EDGE('',*,*,#12600,.F.);
#16434=ORIENTED_EDGE('',*,*,#12601,.F.);
#16435=ORIENTED_EDGE('',*,*,#12598,.F.);
#21154=CYLINDRICAL_SURFACE('',#24717,0.265);
#21155=CYLINDRICAL_SURFACE('',#24721,0.5);
#21987=ADVANCED_FACE('',(#3206),#1449,.F.);
#21988=ADVANCED_FACE('',(#3207),#21154,.F.);
#21989=ADVANCED_FACE('',(#3208,#2046),#2477,.T.);
#21990=ADVANCED_FACE('',(#3209),#21155,.T.);
#21991=ADVANCED_FACE('',(#3210,#2047),#2478,.F.);
#23006=CLOSED_SHELL('',(#21987,#21988,#21989,#21990,#21991));
#24713=AXIS2_PLACEMENT_3D('',#35164,#28284,#28285);
#24714=AXIS2_PLACEMENT_3D('',#35165,#28286,#28287);
#24715=AXIS2_PLACEMENT_3D('',#35167,#28288,#28289);
#24716=AXIS2_PLACEMENT_3D('',#35170,#28291,#28292);
#24717=AXIS2_PLACEMENT_3D('',#35171,#28293,#28294);
#24718=AXIS2_PLACEMENT_3D('',#35174,#28296,#28297);
#24719=AXIS2_PLACEMENT_3D('',#35175,#28298,#28299);
#24720=AXIS2_PLACEMENT_3D('',#35177,#28300,#28301);
#24721=AXIS2_PLACEMENT_3D('',#35178,#28302,#28303);
#24722=AXIS2_PLACEMENT_3D('',#35181,#28305,#28306);
#24723=AXIS2_PLACEMENT_3D('',#35182,#28307,#28308);
#28284=DIRECTION('axis',(0.,0.,1.));
#28285=DIRECTION('refdir',(1.,0.,0.));
#28286=DIRECTION('center_axis',(0.,1.,0.));
#28287=DIRECTION('ref_axis',(1.,0.,0.));
#28288=DIRECTION('center_axis',(0.,1.,0.));
#28289=DIRECTION('ref_axis',(1.,0.,0.));
#28290=DIRECTION('',(0.707106781186548,-0.707106781186547,-8.65956056235494E-17));
#28291=DIRECTION('center_axis',(0.,-1.,0.));
#28292=DIRECTION('ref_axis',(1.,0.,0.));
#28293=DIRECTION('center_axis',(0.,1.,0.));
#28294=DIRECTION('ref_axis',(1.,0.,0.));
#28295=DIRECTION('',(0.,-1.,0.));
#28296=DIRECTION('center_axis',(0.,-1.,0.));
#28297=DIRECTION('ref_axis',(1.,0.,0.));
#28298=DIRECTION('center_axis',(0.,1.,0.));
#28299=DIRECTION('ref_axis',(1.,0.,0.));
#28300=DIRECTION('center_axis',(0.,1.,0.));
#28301=DIRECTION('ref_axis',(1.,0.,0.));
#28302=DIRECTION('center_axis',(0.,1.,0.));
#28303=DIRECTION('ref_axis',(1.,0.,0.));
#28304=DIRECTION('',(0.,-1.,0.));
#28305=DIRECTION('center_axis',(0.,1.,0.));
#28306=DIRECTION('ref_axis',(1.,0.,0.));
#28307=DIRECTION('center_axis',(0.,1.,0.));
#28308=DIRECTION('ref_axis',(1.,0.,0.));
#35164=CARTESIAN_POINT('',(0.,0.,0.));
#35165=CARTESIAN_POINT('Origin',(0.,0.09,0.));
#35166=CARTESIAN_POINT('',(-0.285,0.1,3.49024337756996E-17));
#35167=CARTESIAN_POINT('Origin',(0.,0.1,0.));
#35168=CARTESIAN_POINT('',(-0.265,0.08,-3.24531401774049E-17));
#35169=CARTESIAN_POINT('',(-0.275,0.09,3.36777869765522E-17));
#35170=CARTESIAN_POINT('Origin',(0.,0.08,0.));
#35171=CARTESIAN_POINT('Origin',(0.,0.,0.));
#35172=CARTESIAN_POINT('',(-0.265,0.,3.24531401774049E-17));
#35173=CARTESIAN_POINT('',(-0.265,0.,3.24531401774049E-17));
#35174=CARTESIAN_POINT('Origin',(0.,0.,0.));
#35175=CARTESIAN_POINT('Origin',(0.,0.1,0.));
#35176=CARTESIAN_POINT('',(-0.5,0.1,6.12323399573677E-17));
#35177=CARTESIAN_POINT('Origin',(0.,0.1,0.));
#35178=CARTESIAN_POINT('Origin',(0.,0.,0.));
#35179=CARTESIAN_POINT('',(-0.5,0.,6.12323399573677E-17));
#35180=CARTESIAN_POINT('',(-0.5,0.,6.12323399573677E-17));
#35181=CARTESIAN_POINT('Origin',(0.,0.,0.));
#35182=CARTESIAN_POINT('Origin',(0.,0.,0.));
#62821=UNCERTAINTY_MEASURE_WITH_UNIT(LENGTH_MEASURE(0.001),#62985,
'DISTANCE_ACCURACY_VALUE',
'Maximum model space distance between geometric entities at asserted c
onnectivities');
#62885=UNCERTAINTY_MEASURE_WITH_UNIT(LENGTH_MEASURE(0.001),#62985,
'DISTANCE_ACCURACY_VALUE',
'Maximum model space distance between geometric entities at asserted c
onnectivities');
#62920=(
GEOMETRIC_REPRESENTATION_CONTEXT(3)
GLOBAL_UNCERTAINTY_ASSIGNED_CONTEXT((#62821))
GLOBAL_UNIT_ASSIGNED_CONTEXT((#62985,#62987,#62988))
REPRESENTATION_CONTEXT('','3D')
);
#62984=(
GEOMETRIC_REPRESENTATION_CONTEXT(3)
GLOBAL_UNCERTAINTY_ASSIGNED_CONTEXT((#62885))
GLOBAL_UNIT_ASSIGNED_CONTEXT((#62985,#62987,#62988))
REPRESENTATION_CONTEXT('','3D')
);
#62985=(
LENGTH_UNIT()
NAMED_UNIT(*)
SI_UNIT(.CENTI.,.METRE.)
);
#62987=(
NAMED_UNIT(*)
PLANE_ANGLE_UNIT()
SI_UNIT($,.RADIAN.)
);
#62988=(
NAMED_UNIT(*)
SI_UNIT($,.STERADIAN.)
SOLID_ANGLE_UNIT()
);
#63023=SHAPE_DEFINITION_REPRESENTATION(#63134,#63383);
#63134=PRODUCT_DEFINITION_SHAPE('',$,#63482);
#63383=SHAPE_REPRESENTATION('',(#24713),#62920);
#63447=PRODUCT_DEFINITION_CONTEXT('part definition',#63743,'design');
#63482=PRODUCT_DEFINITION('Flat Washer - M5','Flat Washer - M5',#63580,
#63447);
#63580=PRODUCT_DEFINITION_FORMATION('',$,#63779);
#63743=APPLICATION_CONTEXT(
'Core Data for Automotive Mechanical Design Process');
#63744=PRODUCT_CONTEXT('part definition',#63743,'mechanical');
#63779=PRODUCT('Flat Washer - M5','Flat Washer - M5','Flat Washer - M5',
(#63744));
#63913=COLOUR_RGB('Black',0.12,0.14,0.17);
#63914=FILL_AREA_STYLE_COLOUR('',#63913);
#63915=FILL_AREA_STYLE('',(#63914));
#63916=SURFACE_STYLE_FILL_AREA(#63915);
#63917=SURFACE_SIDE_STYLE('',(#63916));
#63918=SURFACE_STYLE_USAGE(.BOTH.,#63917);
#63919=PRESENTATION_STYLE_ASSIGNMENT((#63918));
ENDSEC;
END-ISO-10303-21;
